ISO-10303-21;
HEADER;
/* Generated by software containing ST-Developer
 * from STEP Tools, Inc. (www.steptools.com) 
 */

FILE_DESCRIPTION(
/* description */ ('Line shaft on three pillow blocks'),
/* implementation_level */ '2;1');

FILE_NAME(
/* name */ 'Mounting reducer bush (2).step',
/* time_stamp */ '2026-10-27T10:49:19-07:00',
/* author */ (''),
/* organization */ (''),
/* preprocessor_version */ 'ST-DEVELOPER v20.2',
/* originating_system */ 'Autodesk Translation Framework v15.17.0.0',
/* authorisation */ '');

FILE_SCHEMA (('AUTOMOTIVE_DESIGN { 1 0 10303 214 3 1 1 }'));
ENDSEC;

DATA;
#10=MECHANICAL_DESIGN_GEOMETRIC_PRESENTATION_REPRESENTATION('',(#345),#8377);
#291=SHAPE_REPRESENTATION_RELATIONSHIP('SRR','None',#8506,#318);
#318=ADVANCED_BREP_SHAPE_REPRESENTATION('',(#373),#8355);
#345=STYLED_ITEM('',(#8732),#373);
#373=MANIFOLD_SOLID_BREP('Body1',#4331);
#419=FACE_BOUND('',#993,.T.);
#420=FACE_BOUND('',#995,.T.);
#526=PLANE('',#4761);
#527=PLANE('',#4762);
#710=FACE_OUTER_BOUND('',#990,.T.);
#711=FACE_OUTER_BOUND('',#991,.T.);
#712=FACE_OUTER_BOUND('',#992,.T.);
#713=FACE_OUTER_BOUND('',#994,.T.);
#990=EDGE_LOOP('',(#3177,#3178,#3179,#3180));
#991=EDGE_LOOP('',(#3181,#3182,#3183,#3184));
#992=EDGE_LOOP('',(#3185));
#993=EDGE_LOOP('',(#3186));
#994=EDGE_LOOP('',(#3187));
#995=EDGE_LOOP('',(#3188));
#1333=LINE('',#6725,#1660);
#1334=LINE('',#6731,#1661);
#1660=VECTOR('',#5434,0.425);
#1661=VECTOR('',#5441,0.645);
#1945=CIRCLE('',#4756,0.425);
#1946=CIRCLE('',#4757,0.425);
#1947=CIRCLE('',#4759,0.645);
#1948=CIRCLE('',#4760,0.645);
#2144=VERTEX_POINT('',#6722);
#2145=VERTEX_POINT('',#6724);
#2146=VERTEX_POINT('',#6728);
#2147=VERTEX_POINT('',#6730);
#2537=EDGE_CURVE('',#2144,#2144,#1945,.T.);
#2538=EDGE_CURVE('',#2144,#2145,#1333,.T.);
#2539=EDGE_CURVE('',#2145,#2145,#1946,.T.);
#2540=EDGE_CURVE('',#2146,#2146,#1947,.T.);
#2541=EDGE_CURVE('',#2146,#2147,#1334,.T.);
#2542=EDGE_CURVE('',#2147,#2147,#1948,.T.);
#3177=ORIENTED_EDGE('',*,*,#2537,.F.);
#3178=ORIENTED_EDGE('',*,*,#2538,.T.);
#3179=ORIENTED_EDGE('',*,*,#2539,.T.);
#3180=ORIENTED_EDGE('',*,*,#2538,.F.);
#3181=ORIENTED_EDGE('',*,*,#2540,.F.);
#3182=ORIENTED_EDGE('',*,*,#2541,.T.);
#3183=ORIENTED_EDGE('',*,*,#2542,.T.);
#3184=ORIENTED_EDGE('',*,*,#2541,.F.);
#3185=ORIENTED_EDGE('',*,*,#2540,.T.);
#3186=ORIENTED_EDGE('',*,*,#2537,.T.);
#3187=ORIENTED_EDGE('',*,*,#2542,.F.);
#3188=ORIENTED_EDGE('',*,*,#2539,.F.);
#4019=CYLINDRICAL_SURFACE('',#4755,0.425);
#4020=CYLINDRICAL_SURFACE('',#4758,0.645);
#4128=ADVANCED_FACE('',(#710),#4019,.F.);
#4129=ADVANCED_FACE('',(#711),#4020,.T.);
#4130=ADVANCED_FACE('',(#712,#419),#526,.T.);
#4131=ADVANCED_FACE('',(#713,#420),#527,.F.);
#4331=CLOSED_SHELL('',(#4128,#4129,#4130,#4131));
#4754=AXIS2_PLACEMENT_3D('',#6720,#5428,#5429);
#4755=AXIS2_PLACEMENT_3D('',#6721,#5430,#5431);
#4756=AXIS2_PLACEMENT_3D('',#6723,#5432,#5433);
#4757=AXIS2_PLACEMENT_3D('',#6726,#5435,#5436);
#4758=AXIS2_PLACEMENT_3D('',#6727,#5437,#5438);
#4759=AXIS2_PLACEMENT_3D('',#6729,#5439,#5440);
#4760=AXIS2_PLACEMENT_3D('',#6732,#5442,#5443);
#4761=AXIS2_PLACEMENT_3D('',#6733,#5444,#5445);
#4762=AXIS2_PLACEMENT_3D('',#6734,#5446,#5447);
#5428=DIRECTION('axis',(0.,0.,1.));
#5429=DIRECTION('refdir',(1.,0.,0.));
#5430=DIRECTION('center_axis',(0.,0.,1.));
#5431=DIRECTION('ref_axis',(1.,0.,0.));
#5432=DIRECTION('center_axis',(0.,0.,-1.));
#5433=DIRECTION('ref_axis',(1.,0.,0.));
#5434=DIRECTION('',(0.,0.,-1.));
#5435=DIRECTION('center_axis',(0.,0.,-1.));
#5436=DIRECTION('ref_axis',(1.,0.,0.));
#5437=DIRECTION('center_axis',(0.,0.,1.));
#5438=DIRECTION('ref_axis',(1.,0.,0.));
#5439=DIRECTION('center_axis',(0.,0.,1.));
#5440=DIRECTION('ref_axis',(1.,0.,0.));
#5441=DIRECTION('',(0.,0.,-1.));
#5442=DIRECTION('center_axis',(0.,0.,1.));
#5443=DIRECTION('ref_axis',(1.,0.,0.));
#5444=DIRECTION('center_axis',(0.,0.,1.));
#5445=DIRECTION('ref_axis',(1.,0.,0.));
#5446=DIRECTION('center_axis',(0.,0.,1.));
#5447=DIRECTION('ref_axis',(1.,0.,0.));
#6720=CARTESIAN_POINT('',(0.,0.,0.));
#6721=CARTESIAN_POINT('Origin',(-4.75,15.,1.2));
#6722=CARTESIAN_POINT('',(-5.175,15.,2.4));
#6723=CARTESIAN_POINT('Origin',(-4.75,15.,2.4));
#6724=CARTESIAN_POINT('',(-5.175,15.,1.2));
#6725=CARTESIAN_POINT('',(-5.175,15.,1.2));
#6726=CARTESIAN_POINT('Origin',(-4.75,15.,1.2));
#6727=CARTESIAN_POINT('Origin',(-4.75,15.,1.2));
#6728=CARTESIAN_POINT('',(-5.395,15.,2.4));
#6729=CARTESIAN_POINT('Origin',(-4.75,15.,2.4));
#6730=CARTESIAN_POINT('',(-5.395,15.,1.2));
#6731=CARTESIAN_POINT('',(-5.395,15.,1.2));
#6732=CARTESIAN_POINT('Origin',(-4.75,15.,1.2));
#6733=CARTESIAN_POINT('Origin',(-4.75,15.,2.4));
#6734=CARTESIAN_POINT('Origin',(-4.75,15.,1.2));
#8323=UNCERTAINTY_MEASURE_WITH_UNIT(LENGTH_MEASURE(0.001),#8378,
'DISTANCE_ACCURACY_VALUE',
'Maximum model space distance between geometric entities at asserted c
onnectivities');
#8345=UNCERTAINTY_MEASURE_WITH_UNIT(LENGTH_MEASURE(0.001),#8378,
'DISTANCE_ACCURACY_VALUE',
'Maximum model space distance between geometric entities at asserted c
onnectivities');
#8355=(
GEOMETRIC_REPRESENTATION_CONTEXT(3)
GLOBAL_UNCERTAINTY_ASSIGNED_CONTEXT((#8323))
GLOBAL_UNIT_ASSIGNED_CONTEXT((#8378,#8380,#8381))
REPRESENTATION_CONTEXT('','3D')
);
#8377=(
GEOMETRIC_REPRESENTATION_CONTEXT(3)
GLOBAL_UNCERTAINTY_ASSIGNED_CONTEXT((#8345))
GLOBAL_UNIT_ASSIGNED_CONTEXT((#8378,#8380,#8381))
REPRESENTATION_CONTEXT('','3D')
);
#8378=(
LENGTH_UNIT()
NAMED_UNIT(*)
SI_UNIT(.CENTI.,.METRE.)
);
#8380=(
NAMED_UNIT(*)
PLANE_ANGLE_UNIT()
SI_UNIT($,.RADIAN.)
);
#8381=(
NAMED_UNIT(*)
SI_UNIT($,.STERADIAN.)
SOLID_ANGLE_UNIT()
);
#8391=SHAPE_DEFINITION_REPRESENTATION(#8422,#8506);
#8422=PRODUCT_DEFINITION_SHAPE('',$,#8538);
#8506=SHAPE_REPRESENTATION('',(#4754),#8355);
#8528=PRODUCT_DEFINITION_CONTEXT('part definition',#8623,'design');
#8538=PRODUCT_DEFINITION('Mounting reducer bush (2)',
'Mounting reducer bush (2)',#8569,#8528);
#8569=PRODUCT_DEFINITION_FORMATION('',$,#8634);
#8623=APPLICATION_CONTEXT(
'Core Data for Automotive Mechanical Design Process');
#8624=PRODUCT_CONTEXT('part definition',#8623,'mechanical');
#8634=PRODUCT('Mounting reducer bush (2)','Mounting reducer bush (2)',
'Mounting reducer bush (2)',(#8624));
#8726=COLOUR_RGB('Off White',0.89,0.88,0.83);
#8727=FILL_AREA_STYLE_COLOUR('',#8726);
#8728=FILL_AREA_STYLE('',(#8727));
#8729=SURFACE_STYLE_FILL_AREA(#8728);
#8730=SURFACE_SIDE_STYLE('',(#8729));
#8731=SURFACE_STYLE_USAGE(.BOTH.,#8730);
#8732=PRESENTATION_STYLE_ASSIGNMENT((#8731));
ENDSEC;
END-ISO-10303-21;
